ISO-10303-21;
HEADER;
/* Generated by software containing ST-Developer
 * from STEP Tools, Inc. (www.steptools.com) 
 */

FILE_DESCRIPTION(
/* description */ ('PAT-001'),
/* implementation_level */ '2;1');

FILE_NAME(
/* name */ 'M5x14 Cap Screw.step',
/* time_stamp */ '2026-10-29T17:07:15-07:00',
/* author */ (''),
/* organization */ (''),
/* preprocessor_version */ 'ST-DEVELOPER v20.2',
/* originating_system */ 'Autodesk Translation Framework v15.17.0.0',
/* authorisation */ '');

FILE_SCHEMA (('AUTOMOTIVE_DESIGN { 1 0 10303 214 3 1 1 }'));
ENDSEC;

DATA;
#10=MECHANICAL_DESIGN_GEOMETRIC_PRESENTATION_REPRESENTATION('',(#398),#9622);
#29=ORIENTED_CLOSED_SHELL('',*,#5223,.F.);
#31=BREP_WITH_VOIDS('Body1',#5224,(#29));
#310=CONICAL_SURFACE('',#5902,0.4,0.785398163397448);
#311=CONICAL_SURFACE('',#5906,0.41,0.785398163397448);
#312=CONICAL_SURFACE('',#5910,0.26,0.463647609000806);
#340=SHAPE_REPRESENTATION_RELATIONSHIP('SRR','None',#9764,#365);
#365=ADVANCED_BREP_SHAPE_REPRESENTATION('',(#31),#9613);
#398=STYLED_ITEM('',(#9969),#31);
#489=FACE_BOUND('',#1285,.T.);
#666=PLANE('',#5890);
#667=PLANE('',#5891);
#668=PLANE('',#5892);
#669=PLANE('',#5893);
#670=PLANE('',#5894);
#671=PLANE('',#5895);
#672=PLANE('',#5896);
#673=PLANE('',#5897);
#674=PLANE('',#5898);
#675=PLANE('',#5900);
#676=PLANE('',#5908);
#923=FACE_OUTER_BOUND('',#1271,.T.);
#924=FACE_OUTER_BOUND('',#1272,.T.);
#925=FACE_OUTER_BOUND('',#1273,.T.);
#926=FACE_OUTER_BOUND('',#1274,.T.);
#927=FACE_OUTER_BOUND('',#1275,.T.);
#928=FACE_OUTER_BOUND('',#1276,.T.);
#929=FACE_OUTER_BOUND('',#1277,.T.);
#930=FACE_OUTER_BOUND('',#1278,.T.);
#931=FACE_OUTER_BOUND('',#1279,.T.);
#932=FACE_OUTER_BOUND('',#1280,.T.);
#933=FACE_OUTER_BOUND('',#1281,.T.);
#934=FACE_OUTER_BOUND('',#1282,.T.);
#935=FACE_OUTER_BOUND('',#1283,.T.);
#936=FACE_OUTER_BOUND('',#1284,.T.);
#937=FACE_OUTER_BOUND('',#1286,.T.);
#938=FACE_OUTER_BOUND('',#1287,.T.);
#1271=EDGE_LOOP('',(#4471,#4472,#4473,#4474));
#1272=EDGE_LOOP('',(#4475,#4476,#4477,#4478));
#1273=EDGE_LOOP('',(#4479,#4480,#4481,#4482));
#1274=EDGE_LOOP('',(#4483,#4484,#4485,#4486));
#1275=EDGE_LOOP('',(#4487,#4488,#4489,#4490));
#1276=EDGE_LOOP('',(#4491,#4492,#4493,#4494));
#1277=EDGE_LOOP('',(#4495,#4496,#4497,#4498,#4499,#4500));
#1278=EDGE_LOOP('',(#4501,#4502,#4503,#4504,#4505,#4506));
#1279=EDGE_LOOP('',(#4507));
#1280=EDGE_LOOP('',(#4508));
#1281=EDGE_LOOP('',(#4509,#4510,#4511,#4512));
#1282=EDGE_LOOP('',(#4513,#4514,#4515,#4516));
#1283=EDGE_LOOP('',(#4517,#4518,#4519,#4520));
#1284=EDGE_LOOP('',(#4521));
#1285=EDGE_LOOP('',(#4522));
#1286=EDGE_LOOP('',(#4523,#4524,#4525,#4526));
#1287=EDGE_LOOP('',(#4527,#4528,#4529,#4530));
#1710=LINE('',#9087,#2115);
#1711=LINE('',#9089,#2116);
#1712=LINE('',#9091,#2117);
#1713=LINE('',#9092,#2118);
#1714=LINE('',#9095,#2119);
#1715=LINE('',#9097,#2120);
#1716=LINE('',#9098,#2121);
#1717=LINE('',#9101,#2122);
#1718=LINE('',#9103,#2123);
#1719=LINE('',#9104,#2124);
#1720=LINE('',#9107,#2125);
#1721=LINE('',#9109,#2126);
#1722=LINE('',#9110,#2127);
#1723=LINE('',#9113,#2128);
#1724=LINE('',#9115,#2129);
#1725=LINE('',#9116,#2130);
#1726=LINE('',#9118,#2131);
#1727=LINE('',#9119,#2132);
#1728=LINE('',#9131,#2133);
#1729=LINE('',#9135,#2134);
#1730=LINE('',#9139,#2135);
#1731=LINE('',#9146,#2136);
#1732=LINE('',#9148,#2137);
#2115=VECTOR('',#7183,1.);
#2116=VECTOR('',#7184,1.);
#2117=VECTOR('',#7185,1.);
#2118=VECTOR('',#7186,1.);
#2119=VECTOR('',#7189,1.);
#2120=VECTOR('',#7190,1.);
#2121=VECTOR('',#7191,1.);
#2122=VECTOR('',#7194,1.);
#2123=VECTOR('',#7195,1.);
#2124=VECTOR('',#7196,1.);
#2125=VECTOR('',#7199,1.);
#2126=VECTOR('',#7200,1.);
#2127=VECTOR('',#7201,1.);
#2128=VECTOR('',#7204,1.);
#2129=VECTOR('',#7205,1.);
#2130=VECTOR('',#7206,1.);
#2131=VECTOR('',#7209,1.);
#2132=VECTOR('',#7210,1.);
#2133=VECTOR('',#7227,0.4);
#2134=VECTOR('',#7232,0.425);
#2135=VECTOR('',#7237,0.41);
#2136=VECTOR('',#7246,0.26);
#2137=VECTOR('',#7249,0.25);
#2353=CIRCLE('',#5899,0.24505);
#2354=CIRCLE('',#5901,0.375);
#2355=CIRCLE('',#5903,0.425);
#2356=CIRCLE('',#5905,0.425);
#2357=CIRCLE('',#5907,0.395);
#2358=CIRCLE('',#5909,0.27);
#2359=CIRCLE('',#5911,0.24505);
#2747=VERTEX_POINT('',#9085);
#2748=VERTEX_POINT('',#9086);
#2749=VERTEX_POINT('',#9088);
#2750=VERTEX_POINT('',#9090);
#2751=VERTEX_POINT('',#9094);
#2752=VERTEX_POINT('',#9096);
#2753=VERTEX_POINT('',#9100);
#2754=VERTEX_POINT('',#9102);
#2755=VERTEX_POINT('',#9106);
#2756=VERTEX_POINT('',#9108);
#2757=VERTEX_POINT('',#9112);
#2758=VERTEX_POINT('',#9114);
#2759=VERTEX_POINT('',#9123);
#2760=VERTEX_POINT('',#9126);
#2761=VERTEX_POINT('',#9129);
#2762=VERTEX_POINT('',#9133);
#2763=VERTEX_POINT('',#9137);
#2764=VERTEX_POINT('',#9141);
#2765=VERTEX_POINT('',#9144);
#3339=EDGE_CURVE('',#2747,#2748,#1710,.T.);
#3340=EDGE_CURVE('',#2748,#2749,#1711,.T.);
#3341=EDGE_CURVE('',#2749,#2750,#1712,.T.);
#3342=EDGE_CURVE('',#2747,#2750,#1713,.T.);
#3343=EDGE_CURVE('',#2748,#2751,#1714,.T.);
#3344=EDGE_CURVE('',#2751,#2752,#1715,.T.);
#3345=EDGE_CURVE('',#2752,#2749,#1716,.T.);
#3346=EDGE_CURVE('',#2751,#2753,#1717,.T.);
#3347=EDGE_CURVE('',#2753,#2754,#1718,.T.);
#3348=EDGE_CURVE('',#2754,#2752,#1719,.T.);
#3349=EDGE_CURVE('',#2753,#2755,#1720,.T.);
#3350=EDGE_CURVE('',#2755,#2756,#1721,.T.);
#3351=EDGE_CURVE('',#2756,#2754,#1722,.T.);
#3352=EDGE_CURVE('',#2755,#2757,#1723,.T.);
#3353=EDGE_CURVE('',#2757,#2758,#1724,.T.);
#3354=EDGE_CURVE('',#2758,#2756,#1725,.T.);
#3355=EDGE_CURVE('',#2757,#2747,#1726,.T.);
#3356=EDGE_CURVE('',#2750,#2758,#1727,.T.);
#3357=EDGE_CURVE('',#2759,#2759,#2353,.T.);
#3358=EDGE_CURVE('',#2760,#2760,#2354,.T.);
#3359=EDGE_CURVE('',#2761,#2761,#2355,.T.);
#3360=EDGE_CURVE('',#2761,#2760,#1728,.T.);
#3361=EDGE_CURVE('',#2762,#2762,#2356,.T.);
#3362=EDGE_CURVE('',#2762,#2761,#1729,.T.);
#3363=EDGE_CURVE('',#2763,#2763,#2357,.T.);
#3364=EDGE_CURVE('',#2763,#2762,#1730,.T.);
#3365=EDGE_CURVE('',#2764,#2764,#2358,.T.);
#3366=EDGE_CURVE('',#2765,#2765,#2359,.F.);
#3367=EDGE_CURVE('',#2765,#2764,#1731,.T.);
#3368=EDGE_CURVE('',#2759,#2765,#1732,.T.);
#4471=ORIENTED_EDGE('',*,*,#3339,.T.);
#4472=ORIENTED_EDGE('',*,*,#3340,.T.);
#4473=ORIENTED_EDGE('',*,*,#3341,.T.);
#4474=ORIENTED_EDGE('',*,*,#3342,.F.);
#4475=ORIENTED_EDGE('',*,*,#3343,.T.);
#4476=ORIENTED_EDGE('',*,*,#3344,.T.);
#4477=ORIENTED_EDGE('',*,*,#3345,.T.);
#4478=ORIENTED_EDGE('',*,*,#3340,.F.);
#4479=ORIENTED_EDGE('',*,*,#3346,.T.);
#4480=ORIENTED_EDGE('',*,*,#3347,.T.);
#4481=ORIENTED_EDGE('',*,*,#3348,.T.);
#4482=ORIENTED_EDGE('',*,*,#3344,.F.);
#4483=ORIENTED_EDGE('',*,*,#3349,.T.);
#4484=ORIENTED_EDGE('',*,*,#3350,.T.);
#4485=ORIENTED_EDGE('',*,*,#3351,.T.);
#4486=ORIENTED_EDGE('',*,*,#3347,.F.);
#4487=ORIENTED_EDGE('',*,*,#3352,.T.);
#4488=ORIENTED_EDGE('',*,*,#3353,.T.);
#4489=ORIENTED_EDGE('',*,*,#3354,.T.);
#4490=ORIENTED_EDGE('',*,*,#3350,.F.);
#4491=ORIENTED_EDGE('',*,*,#3355,.T.);
#4492=ORIENTED_EDGE('',*,*,#3342,.T.);
#4493=ORIENTED_EDGE('',*,*,#3356,.T.);
#4494=ORIENTED_EDGE('',*,*,#3353,.F.);
#4495=ORIENTED_EDGE('',*,*,#3355,.F.);
#4496=ORIENTED_EDGE('',*,*,#3352,.F.);
#4497=ORIENTED_EDGE('',*,*,#3349,.F.);
#4498=ORIENTED_EDGE('',*,*,#3346,.F.);
#4499=ORIENTED_EDGE('',*,*,#3343,.F.);
#4500=ORIENTED_EDGE('',*,*,#3339,.F.);
#4501=ORIENTED_EDGE('',*,*,#3356,.F.);
#4502=ORIENTED_EDGE('',*,*,#3341,.F.);
#4503=ORIENTED_EDGE('',*,*,#3345,.F.);
#4504=ORIENTED_EDGE('',*,*,#3348,.F.);
#4505=ORIENTED_EDGE('',*,*,#3351,.F.);
#4506=ORIENTED_EDGE('',*,*,#3354,.F.);
#4507=ORIENTED_EDGE('',*,*,#3357,.F.);
#4508=ORIENTED_EDGE('',*,*,#3358,.F.);
#4509=ORIENTED_EDGE('',*,*,#3359,.F.);
#4510=ORIENTED_EDGE('',*,*,#3360,.T.);
#4511=ORIENTED_EDGE('',*,*,#3358,.T.);
#4512=ORIENTED_EDGE('',*,*,#3360,.F.);
#4513=ORIENTED_EDGE('',*,*,#3361,.F.);
#4514=ORIENTED_EDGE('',*,*,#3362,.T.);
#4515=ORIENTED_EDGE('',*,*,#3359,.T.);
#4516=ORIENTED_EDGE('',*,*,#3362,.F.);
#4517=ORIENTED_EDGE('',*,*,#3363,.F.);
#4518=ORIENTED_EDGE('',*,*,#3364,.T.);
#4519=ORIENTED_EDGE('',*,*,#3361,.T.);
#4520=ORIENTED_EDGE('',*,*,#3364,.F.);
#4521=ORIENTED_EDGE('',*,*,#3363,.T.);
#4522=ORIENTED_EDGE('',*,*,#3365,.F.);
#4523=ORIENTED_EDGE('',*,*,#3366,.F.);
#4524=ORIENTED_EDGE('',*,*,#3367,.T.);
#4525=ORIENTED_EDGE('',*,*,#3365,.T.);
#4526=ORIENTED_EDGE('',*,*,#3367,.F.);
#4527=ORIENTED_EDGE('',*,*,#3357,.T.);
#4528=ORIENTED_EDGE('',*,*,#3368,.T.);
#4529=ORIENTED_EDGE('',*,*,#3366,.T.);
#4530=ORIENTED_EDGE('',*,*,#3368,.F.);
#4874=CYLINDRICAL_SURFACE('',#5904,0.425);
#4875=CYLINDRICAL_SURFACE('',#5912,0.24505);
#5110=ADVANCED_FACE('',(#923),#666,.F.);
#5111=ADVANCED_FACE('',(#924),#667,.F.);
#5112=ADVANCED_FACE('',(#925),#668,.F.);
#5113=ADVANCED_FACE('',(#926),#669,.F.);
#5114=ADVANCED_FACE('',(#927),#670,.F.);
#5115=ADVANCED_FACE('',(#928),#671,.F.);
#5116=ADVANCED_FACE('',(#929),#672,.F.);
#5117=ADVANCED_FACE('',(#930),#673,.F.);
#5118=ADVANCED_FACE('',(#931),#674,.F.);
#5119=ADVANCED_FACE('',(#932),#675,.T.);
#5120=ADVANCED_FACE('',(#933),#310,.T.);
#5121=ADVANCED_FACE('',(#934),#4874,.T.);
#5122=ADVANCED_FACE('',(#935),#311,.T.);
#5123=ADVANCED_FACE('',(#936,#489),#676,.T.);
#5124=ADVANCED_FACE('',(#937),#312,.T.);
#5125=ADVANCED_FACE('',(#938),#4875,.T.);
#5223=CLOSED_SHELL('',(#5110,#5111,#5112,#5113,#5114,#5115,#5116,#5117));
#5224=CLOSED_SHELL('',(#5118,#5119,#5120,#5121,#5122,#5123,#5124,#5125));
#5889=AXIS2_PLACEMENT_3D('',#9083,#7179,#7180);
#5890=AXIS2_PLACEMENT_3D('',#9084,#7181,#7182);
#5891=AXIS2_PLACEMENT_3D('',#9093,#7187,#7188);
#5892=AXIS2_PLACEMENT_3D('',#9099,#7192,#7193);
#5893=AXIS2_PLACEMENT_3D('',#9105,#7197,#7198);
#5894=AXIS2_PLACEMENT_3D('',#9111,#7202,#7203);
#5895=AXIS2_PLACEMENT_3D('',#9117,#7207,#7208);
#5896=AXIS2_PLACEMENT_3D('',#9120,#7211,#7212);
#5897=AXIS2_PLACEMENT_3D('',#9121,#7213,#7214);
#5898=AXIS2_PLACEMENT_3D('',#9122,#7215,#7216);
#5899=AXIS2_PLACEMENT_3D('',#9124,#7217,#7218);
#5900=AXIS2_PLACEMENT_3D('',#9125,#7219,#7220);
#5901=AXIS2_PLACEMENT_3D('',#9127,#7221,#7222);
#5902=AXIS2_PLACEMENT_3D('',#9128,#7223,#7224);
#5903=AXIS2_PLACEMENT_3D('',#9130,#7225,#7226);
#5904=AXIS2_PLACEMENT_3D('',#9132,#7228,#7229);
#5905=AXIS2_PLACEMENT_3D('',#9134,#7230,#7231);
#5906=AXIS2_PLACEMENT_3D('',#9136,#7233,#7234);
#5907=AXIS2_PLACEMENT_3D('',#9138,#7235,#7236);
#5908=AXIS2_PLACEMENT_3D('',#9140,#7238,#7239);
#5909=AXIS2_PLACEMENT_3D('',#9142,#7240,#7241);
#5910=AXIS2_PLACEMENT_3D('',#9143,#7242,#7243);
#5911=AXIS2_PLACEMENT_3D('',#9145,#7244,#7245);
#5912=AXIS2_PLACEMENT_3D('',#9147,#7247,#7248);
#7179=DIRECTION('axis',(0.,0.,1.));
#7180=DIRECTION('refdir',(1.,0.,0.));
#7181=DIRECTION('center_axis',(0.866025403784439,0.,-0.5));
#7182=DIRECTION('ref_axis',(0.5,0.,0.866025403784439));
#7183=DIRECTION('',(-0.5,0.,-0.866025403784439));
#7184=DIRECTION('',(0.,-1.,0.));
#7185=DIRECTION('',(0.5,0.,0.866025403784439));
#7186=DIRECTION('',(0.,-1.,0.));
#7187=DIRECTION('center_axis',(1.20185167898973E-16,0.,-1.));
#7188=DIRECTION('ref_axis',(1.,0.,1.20185167898973E-16));
#7189=DIRECTION('',(-1.,0.,-1.20185167898973E-16));
#7190=DIRECTION('',(0.,-1.,0.));
#7191=DIRECTION('',(1.,0.,1.20185167898973E-16));
#7192=DIRECTION('center_axis',(-0.866025403784439,0.,-0.5));
#7193=DIRECTION('ref_axis',(0.5,0.,-0.866025403784439));
#7194=DIRECTION('',(-0.5,0.,0.866025403784439));
#7195=DIRECTION('',(0.,-1.,0.));
#7196=DIRECTION('',(0.5,0.,-0.866025403784439));
#7197=DIRECTION('center_axis',(-0.866025403784439,0.,0.5));
#7198=DIRECTION('ref_axis',(-0.5,0.,-0.866025403784439));
#7199=DIRECTION('',(0.5,0.,0.866025403784439));
#7200=DIRECTION('',(0.,-1.,0.));
#7201=DIRECTION('',(-0.5,0.,-0.866025403784439));
#7202=DIRECTION('center_axis',(-2.40370335797945E-16,0.,1.));
#7203=DIRECTION('ref_axis',(-1.,0.,-2.40370335797945E-16));
#7204=DIRECTION('',(1.,0.,2.40370335797945E-16));
#7205=DIRECTION('',(0.,-1.,0.));
#7206=DIRECTION('',(-1.,0.,-2.40370335797945E-16));
#7207=DIRECTION('center_axis',(0.866025403784439,0.,0.5));
#7208=DIRECTION('ref_axis',(-0.5,0.,0.866025403784439));
#7209=DIRECTION('',(0.5,0.,-0.866025403784439));
#7210=DIRECTION('',(-0.5,0.,0.866025403784439));
#7211=DIRECTION('center_axis',(0.,1.,0.));
#7212=DIRECTION('ref_axis',(1.,0.,0.));
#7213=DIRECTION('center_axis',(0.,-1.,0.));
#7214=DIRECTION('ref_axis',(0.,0.,-1.));
#7215=DIRECTION('center_axis',(0.,1.,0.));
#7216=DIRECTION('ref_axis',(1.,0.,0.));
#7217=DIRECTION('center_axis',(0.,1.,0.));
#7218=DIRECTION('ref_axis',(1.,0.,0.));
#7219=DIRECTION('center_axis',(0.,1.,0.));
#7220=DIRECTION('ref_axis',(0.,0.,1.));
#7221=DIRECTION('center_axis',(0.,-1.,0.));
#7222=DIRECTION('ref_axis',(1.,0.,0.));
#7223=DIRECTION('center_axis',(0.,-1.,0.));
#7224=DIRECTION('ref_axis',(1.,0.,0.));
#7225=DIRECTION('center_axis',(0.,-1.,0.));
#7226=DIRECTION('ref_axis',(1.,0.,0.));
#7227=DIRECTION('',(0.707106781186548,0.707106781186547,8.65956056235493E-17));
#7228=DIRECTION('center_axis',(0.,-1.,0.));
#7229=DIRECTION('ref_axis',(1.,0.,0.));
#7230=DIRECTION('center_axis',(0.,-1.,0.));
#7231=DIRECTION('ref_axis',(1.,0.,0.));
#7232=DIRECTION('',(0.,1.,0.));
#7233=DIRECTION('center_axis',(0.,1.,0.));
#7234=DIRECTION('ref_axis',(1.,0.,0.));
#7235=DIRECTION('center_axis',(0.,-1.,0.));
#7236=DIRECTION('ref_axis',(1.,0.,0.));
#7237=DIRECTION('',(-0.707106781186547,0.707106781186548,-8.65956056235493E-17));
#7238=DIRECTION('center_axis',(0.,-1.,0.));
#7239=DIRECTION('ref_axis',(0.,0.,-1.));
#7240=DIRECTION('center_axis',(0.,-1.,0.));
#7241=DIRECTION('ref_axis',(1.,0.,0.));
#7242=DIRECTION('center_axis',(0.,1.,0.));
#7243=DIRECTION('ref_axis',(1.,0.,0.));
#7244=DIRECTION('center_axis',(0.,1.,0.));
#7245=DIRECTION('ref_axis',(1.,0.,0.));
#7246=DIRECTION('',(-0.447213595499958,0.894427190999916,-5.47678698264203E-17));
#7247=DIRECTION('center_axis',(0.,-1.,0.));
#7248=DIRECTION('ref_axis',(1.,0.,0.));
#7249=DIRECTION('',(0.,1.,0.));
#9083=CARTESIAN_POINT('',(0.,0.,0.));
#9084=CARTESIAN_POINT('Origin',(0.115470053837925,-0.5,-0.2));
#9085=CARTESIAN_POINT('',(0.23094010767585,-0.5,0.));
#9086=CARTESIAN_POINT('',(0.115470053837925,-0.5,-0.2));
#9087=CARTESIAN_POINT('',(0.23094010767585,-0.5,0.));
#9088=CARTESIAN_POINT('',(0.115470053837925,-0.8,-0.2));
#9089=CARTESIAN_POINT('',(0.115470053837925,-0.5,-0.2));
#9090=CARTESIAN_POINT('',(0.23094010767585,-0.8,0.));
#9091=CARTESIAN_POINT('',(0.23094010767585,-0.8,0.));
#9092=CARTESIAN_POINT('',(0.23094010767585,-0.5,0.));
#9093=CARTESIAN_POINT('Origin',(-0.115470053837925,-0.5,-0.2));
#9094=CARTESIAN_POINT('',(-0.115470053837925,-0.5,-0.2));
#9095=CARTESIAN_POINT('',(0.115470053837925,-0.5,-0.2));
#9096=CARTESIAN_POINT('',(-0.115470053837925,-0.8,-0.2));
#9097=CARTESIAN_POINT('',(-0.115470053837925,-0.5,-0.2));
#9098=CARTESIAN_POINT('',(0.115470053837925,-0.8,-0.2));
#9099=CARTESIAN_POINT('Origin',(-0.23094010767585,-0.5,-2.77555756156289E-17));
#9100=CARTESIAN_POINT('',(-0.23094010767585,-0.5,-2.82820063659975E-17));
#9101=CARTESIAN_POINT('',(-0.115470053837925,-0.5,-0.2));
#9102=CARTESIAN_POINT('',(-0.23094010767585,-0.8,-2.77555756156289E-17));
#9103=CARTESIAN_POINT('',(-0.23094010767585,-0.5,-2.82820063659975E-17));
#9104=CARTESIAN_POINT('',(-0.115470053837925,-0.8,-0.2));
#9105=CARTESIAN_POINT('Origin',(-0.115470053837925,-0.5,0.2));
#9106=CARTESIAN_POINT('',(-0.115470053837925,-0.5,0.2));
#9107=CARTESIAN_POINT('',(-0.23094010767585,-0.5,-2.82820063659975E-17));
#9108=CARTESIAN_POINT('',(-0.115470053837925,-0.8,0.2));
#9109=CARTESIAN_POINT('',(-0.115470053837925,-0.5,0.2));
#9110=CARTESIAN_POINT('',(-0.23094010767585,-0.8,-2.82820063659975E-17));
#9111=CARTESIAN_POINT('Origin',(0.115470053837925,-0.5,0.2));
#9112=CARTESIAN_POINT('',(0.115470053837925,-0.5,0.2));
#9113=CARTESIAN_POINT('',(-0.115470053837925,-0.5,0.2));
#9114=CARTESIAN_POINT('',(0.115470053837925,-0.8,0.2));
#9115=CARTESIAN_POINT('',(0.115470053837925,-0.5,0.2));
#9116=CARTESIAN_POINT('',(-0.115470053837925,-0.8,0.2));
#9117=CARTESIAN_POINT('Origin',(0.23094010767585,-0.5,0.));
#9118=CARTESIAN_POINT('',(0.115470053837925,-0.5,0.2));
#9119=CARTESIAN_POINT('',(0.115470053837925,-0.8,0.2));
#9120=CARTESIAN_POINT('Origin',(0.,-0.5,0.));
#9121=CARTESIAN_POINT('Origin',(0.,-0.8,0.));
#9122=CARTESIAN_POINT('Origin',(0.,-1.4,0.));
#9123=CARTESIAN_POINT('',(-0.24505,-1.4,3.00099698131059E-17));
#9124=CARTESIAN_POINT('Origin',(0.,-1.4,0.));
#9125=CARTESIAN_POINT('Origin',(0.375,0.5,0.));
#9126=CARTESIAN_POINT('',(-0.375,0.5,-4.59242549680257E-17));
#9127=CARTESIAN_POINT('Origin',(0.,0.5,0.));
#9128=CARTESIAN_POINT('Origin',(0.,0.475,0.));
#9129=CARTESIAN_POINT('',(-0.425,0.45,-5.20474889637625E-17));
#9130=CARTESIAN_POINT('Origin',(0.,0.45,0.));
#9131=CARTESIAN_POINT('',(-0.4,0.475,-4.89858719658941E-17));
#9132=CARTESIAN_POINT('Origin',(0.,0.24,0.));
#9133=CARTESIAN_POINT('',(-0.425,0.0299999999999998,-5.20474889637625E-17));
#9134=CARTESIAN_POINT('Origin',(0.,0.0299999999999998,0.));
#9135=CARTESIAN_POINT('',(-0.425,0.24,-5.20474889637625E-17));
#9136=CARTESIAN_POINT('Origin',(0.,0.0150000000000001,0.));
#9137=CARTESIAN_POINT('',(-0.395,4.85722573273506E-17,-4.83735485663204E-17));
#9138=CARTESIAN_POINT('Origin',(0.,0.,0.));
#9139=CARTESIAN_POINT('',(-0.41,0.0150000000000001,-5.02105187650415E-17));
#9140=CARTESIAN_POINT('Origin',(0.27,0.,0.));
#9141=CARTESIAN_POINT('',(-0.27,0.,-3.30654635769785E-17));
#9142=CARTESIAN_POINT('Origin',(0.,0.,0.));
#9143=CARTESIAN_POINT('Origin',(0.,-0.02,0.));
#9144=CARTESIAN_POINT('',(-0.24505,-0.0498999999999999,3.00099698131059E-17));
#9145=CARTESIAN_POINT('Origin',(0.,-0.0498999999999999,0.));
#9146=CARTESIAN_POINT('',(-0.26,-0.02,-3.18408167778312E-17));
#9147=CARTESIAN_POINT('Origin',(0.,-0.995,0.));
#9148=CARTESIAN_POINT('',(-0.24505,-0.995,-3.00099698131059E-17));
#9583=UNCERTAINTY_MEASURE_WITH_UNIT(LENGTH_MEASURE(0.001),#9623,
'DISTANCE_ACCURACY_VALUE',
'Maximum model space distance between geometric entities at asserted c
onnectivities');
#9592=UNCERTAINTY_MEASURE_WITH_UNIT(LENGTH_MEASURE(0.001),#9623,
'DISTANCE_ACCURACY_VALUE',
'Maximum model space distance between geometric entities at asserted c
onnectivities');
#9613=(
GEOMETRIC_REPRESENTATION_CONTEXT(3)
GLOBAL_UNCERTAINTY_ASSIGNED_CONTEXT((#9583))
GLOBAL_UNIT_ASSIGNED_CONTEXT((#9623,#9625,#9626))
REPRESENTATION_CONTEXT('','3D')
);
#9622=(
GEOMETRIC_REPRESENTATION_CONTEXT(3)
GLOBAL_UNCERTAINTY_ASSIGNED_CONTEXT((#9592))
GLOBAL_UNIT_ASSIGNED_CONTEXT((#9623,#9625,#9626))
REPRESENTATION_CONTEXT('','3D')
);
#9623=(
LENGTH_UNIT()
NAMED_UNIT(*)
SI_UNIT(.CENTI.,.METRE.)
);
#9625=(
NAMED_UNIT(*)
PLANE_ANGLE_UNIT()
SI_UNIT($,.RADIAN.)
);
#9626=(
NAMED_UNIT(*)
SI_UNIT($,.STERADIAN.)
SOLID_ANGLE_UNIT()
);
#9647=SHAPE_DEFINITION_REPRESENTATION(#9681,#9764);
#9681=PRODUCT_DEFINITION_SHAPE('',$,#9794);
#9764=SHAPE_REPRESENTATION('',(#5889),#9613);
#9773=PRODUCT_DEFINITION_CONTEXT('part definition',#9862,'design');
#9794=PRODUCT_DEFINITION('M5x14 Cap Screw','M5x14 Cap Screw',#9823,#9773);
#9823=PRODUCT_DEFINITION_FORMATION('',$,#9884);
#9862=APPLICATION_CONTEXT(
'Core Data for Automotive Mechanical Design Process');
#9863=PRODUCT_CONTEXT('part definition',#9862,'mechanical');
#9884=PRODUCT('M5x14 Cap Screw','M5x14 Cap Screw','M5x14 Cap Screw',(#9863));
#9963=COLOUR_RGB('Black',0.12,0.14,0.17);
#9964=FILL_AREA_STYLE_COLOUR('',#9963);
#9965=FILL_AREA_STYLE('',(#9964));
#9966=SURFACE_STYLE_FILL_AREA(#9965);
#9967=SURFACE_SIDE_STYLE('',(#9966));
#9968=SURFACE_STYLE_USAGE(.BOTH.,#9967);
#9969=PRESENTATION_STYLE_ASSIGNMENT((#9968));
ENDSEC;
END-ISO-10303-21;
